ISO-10303-21;
HEADER;
/* Generated by software containing ST-Developer
 * from STEP Tools, Inc. (www.steptools.com) 
 */

FILE_DESCRIPTION(
/* description */ ('Overhung pulley bearing cartridge'),
/* implementation_level */ '2;1');

FILE_NAME(
/* name */ 'Cap Screw - M4x16.step',
/* time_stamp */ '2026-10-28T03:22:33-07:00',
/* author */ (''),
/* organization */ (''),
/* preprocessor_version */ 'ST-DEVELOPER v20.2',
/* originating_system */ 'Autodesk Translation Framework v15.17.0.0',
/* authorisation */ '');

FILE_SCHEMA (('AUTOMOTIVE_DESIGN { 1 0 10303 214 3 1 1 }'));
ENDSEC;

DATA;
#10=MECHANICAL_DESIGN_GEOMETRIC_PRESENTATION_REPRESENTATION('',(#305),#10963);
#12=ORIENTED_CLOSED_SHELL('',*,#5674,.F.);
#14=BREP_WITH_VOIDS('Body1',#5673,(#12));
#231=CONICAL_SURFACE('',#6274,0.325,0.785398163397448);
#232=CONICAL_SURFACE('',#6278,0.335,0.785398163397448);
#233=CONICAL_SURFACE('',#6282,0.21,0.463647609000806);
#234=CONICAL_SURFACE('',#6286,0.18,0.785398163397448);
#253=SHAPE_REPRESENTATION_RELATIONSHIP('SRR','None',#11074,#275);
#275=ADVANCED_BREP_SHAPE_REPRESENTATION('',(#14),#10954);
#305=STYLED_ITEM('',(#11260),#14);
#406=FACE_BOUND('',#1138,.T.);
#519=PLANE('',#6272);
#520=PLANE('',#6280);
#521=PLANE('',#6288);
#522=PLANE('',#6289);
#523=PLANE('',#6290);
#524=PLANE('',#6291);
#525=PLANE('',#6292);
#526=PLANE('',#6293);
#527=PLANE('',#6294);
#528=PLANE('',#6295);
#529=PLANE('',#6296);
#739=FACE_OUTER_BOUND('',#1133,.T.);
#740=FACE_OUTER_BOUND('',#1134,.T.);
#741=FACE_OUTER_BOUND('',#1135,.T.);
#742=FACE_OUTER_BOUND('',#1136,.T.);
#743=FACE_OUTER_BOUND('',#1137,.T.);
#744=FACE_OUTER_BOUND('',#1139,.T.);
#745=FACE_OUTER_BOUND('',#1140,.T.);
#746=FACE_OUTER_BOUND('',#1141,.T.);
#747=FACE_OUTER_BOUND('',#1142,.T.);
#748=FACE_OUTER_BOUND('',#1143,.T.);
#749=FACE_OUTER_BOUND('',#1144,.T.);
#750=FACE_OUTER_BOUND('',#1145,.T.);
#751=FACE_OUTER_BOUND('',#1146,.T.);
#752=FACE_OUTER_BOUND('',#1147,.T.);
#753=FACE_OUTER_BOUND('',#1148,.T.);
#754=FACE_OUTER_BOUND('',#1149,.T.);
#755=FACE_OUTER_BOUND('',#1150,.T.);
#1133=EDGE_LOOP('',(#4311));
#1134=EDGE_LOOP('',(#4312,#4313,#4314,#4315));
#1135=EDGE_LOOP('',(#4316,#4317,#4318,#4319));
#1136=EDGE_LOOP('',(#4320,#4321,#4322,#4323));
#1137=EDGE_LOOP('',(#4324));
#1138=EDGE_LOOP('',(#4325));
#1139=EDGE_LOOP('',(#4326,#4327,#4328,#4329));
#1140=EDGE_LOOP('',(#4330,#4331,#4332,#4333));
#1141=EDGE_LOOP('',(#4334,#4335,#4336,#4337));
#1142=EDGE_LOOP('',(#4338));
#1143=EDGE_LOOP('',(#4339,#4340,#4341,#4342));
#1144=EDGE_LOOP('',(#4343,#4344,#4345,#4346));
#1145=EDGE_LOOP('',(#4347,#4348,#4349,#4350));
#1146=EDGE_LOOP('',(#4351,#4352,#4353,#4354));
#1147=EDGE_LOOP('',(#4355,#4356,#4357,#4358));
#1148=EDGE_LOOP('',(#4359,#4360,#4361,#4362));
#1149=EDGE_LOOP('',(#4363,#4364,#4365,#4366,#4367,#4368));
#1150=EDGE_LOOP('',(#4369,#4370,#4371,#4372,#4373,#4374));
#1477=LINE('',#9640,#1819);
#1478=LINE('',#9644,#1820);
#1479=LINE('',#9648,#1821);
#1480=LINE('',#9655,#1822);
#1481=LINE('',#9659,#1823);
#1482=LINE('',#9663,#1824);
#1483=LINE('',#9668,#1825);
#1484=LINE('',#9670,#1826);
#1485=LINE('',#9672,#1827);
#1486=LINE('',#9673,#1828);
#1487=LINE('',#9676,#1829);
#1488=LINE('',#9678,#1830);
#1489=LINE('',#9679,#1831);
#1490=LINE('',#9682,#1832);
#1491=LINE('',#9684,#1833);
#1492=LINE('',#9685,#1834);
#1493=LINE('',#9688,#1835);
#1494=LINE('',#9690,#1836);
#1495=LINE('',#9691,#1837);
#1496=LINE('',#9694,#1838);
#1497=LINE('',#9696,#1839);
#1498=LINE('',#9697,#1840);
#1499=LINE('',#9699,#1841);
#1500=LINE('',#9700,#1842);
#1819=VECTOR('',#7539,0.325);
#1820=VECTOR('',#7544,0.35);
#1821=VECTOR('',#7549,0.335);
#1822=VECTOR('',#7558,0.21);
#1823=VECTOR('',#7563,0.2);
#1824=VECTOR('',#7568,0.18);
#1825=VECTOR('',#7573,1.);
#1826=VECTOR('',#7574,1.);
#1827=VECTOR('',#7575,1.);
#1828=VECTOR('',#7576,1.);
#1829=VECTOR('',#7579,1.);
#1830=VECTOR('',#7580,1.);
#1831=VECTOR('',#7581,1.);
#1832=VECTOR('',#7584,1.);
#1833=VECTOR('',#7585,1.);
#1834=VECTOR('',#7586,1.);
#1835=VECTOR('',#7589,1.);
#1836=VECTOR('',#7590,1.);
#1837=VECTOR('',#7591,1.);
#1838=VECTOR('',#7594,1.);
#1839=VECTOR('',#7595,1.);
#1840=VECTOR('',#7596,1.);
#1841=VECTOR('',#7599,1.);
#1842=VECTOR('',#7600,1.);
#2174=CIRCLE('',#6273,0.3);
#2175=CIRCLE('',#6275,0.35);
#2176=CIRCLE('',#6277,0.35);
#2177=CIRCLE('',#6279,0.32);
#2178=CIRCLE('',#6281,0.22);
#2179=CIRCLE('',#6283,0.1954);
#2180=CIRCLE('',#6285,0.1954);
#2181=CIRCLE('',#6287,0.16);
#2609=VERTEX_POINT('',#9635);
#2610=VERTEX_POINT('',#9638);
#2611=VERTEX_POINT('',#9642);
#2612=VERTEX_POINT('',#9646);
#2613=VERTEX_POINT('',#9650);
#2614=VERTEX_POINT('',#9653);
#2615=VERTEX_POINT('',#9657);
#2616=VERTEX_POINT('',#9661);
#2617=VERTEX_POINT('',#9666);
#2618=VERTEX_POINT('',#9667);
#2619=VERTEX_POINT('',#9669);
#2620=VERTEX_POINT('',#9671);
#2621=VERTEX_POINT('',#9675);
#2622=VERTEX_POINT('',#9677);
#2623=VERTEX_POINT('',#9681);
#2624=VERTEX_POINT('',#9683);
#2625=VERTEX_POINT('',#9687);
#2626=VERTEX_POINT('',#9689);
#2627=VERTEX_POINT('',#9693);
#2628=VERTEX_POINT('',#9695);
#3225=EDGE_CURVE('',#2609,#2609,#2174,.T.);
#3226=EDGE_CURVE('',#2610,#2610,#2175,.T.);
#3227=EDGE_CURVE('',#2610,#2609,#1477,.T.);
#3228=EDGE_CURVE('',#2611,#2611,#2176,.T.);
#3229=EDGE_CURVE('',#2611,#2610,#1478,.T.);
#3230=EDGE_CURVE('',#2612,#2612,#2177,.T.);
#3231=EDGE_CURVE('',#2612,#2611,#1479,.T.);
#3232=EDGE_CURVE('',#2613,#2613,#2178,.T.);
#3233=EDGE_CURVE('',#2614,#2614,#2179,.F.);
#3234=EDGE_CURVE('',#2614,#2613,#1480,.T.);
#3235=EDGE_CURVE('',#2615,#2615,#2180,.F.);
#3236=EDGE_CURVE('',#2615,#2614,#1481,.T.);
#3237=EDGE_CURVE('',#2616,#2616,#2181,.T.);
#3238=EDGE_CURVE('',#2616,#2615,#1482,.T.);
#3239=EDGE_CURVE('',#2617,#2618,#1483,.T.);
#3240=EDGE_CURVE('',#2618,#2619,#1484,.T.);
#3241=EDGE_CURVE('',#2619,#2620,#1485,.T.);
#3242=EDGE_CURVE('',#2617,#2620,#1486,.T.);
#3243=EDGE_CURVE('',#2618,#2621,#1487,.T.);
#3244=EDGE_CURVE('',#2621,#2622,#1488,.T.);
#3245=EDGE_CURVE('',#2622,#2619,#1489,.T.);
#3246=EDGE_CURVE('',#2621,#2623,#1490,.T.);
#3247=EDGE_CURVE('',#2623,#2624,#1491,.T.);
#3248=EDGE_CURVE('',#2624,#2622,#1492,.T.);
#3249=EDGE_CURVE('',#2623,#2625,#1493,.T.);
#3250=EDGE_CURVE('',#2625,#2626,#1494,.T.);
#3251=EDGE_CURVE('',#2626,#2624,#1495,.T.);
#3252=EDGE_CURVE('',#2625,#2627,#1496,.T.);
#3253=EDGE_CURVE('',#2627,#2628,#1497,.T.);
#3254=EDGE_CURVE('',#2628,#2626,#1498,.T.);
#3255=EDGE_CURVE('',#2627,#2617,#1499,.T.);
#3256=EDGE_CURVE('',#2620,#2628,#1500,.T.);
#4311=ORIENTED_EDGE('',*,*,#3225,.F.);
#4312=ORIENTED_EDGE('',*,*,#3226,.F.);
#4313=ORIENTED_EDGE('',*,*,#3227,.T.);
#4314=ORIENTED_EDGE('',*,*,#3225,.T.);
#4315=ORIENTED_EDGE('',*,*,#3227,.F.);
#4316=ORIENTED_EDGE('',*,*,#3228,.F.);
#4317=ORIENTED_EDGE('',*,*,#3229,.T.);
#4318=ORIENTED_EDGE('',*,*,#3226,.T.);
#4319=ORIENTED_EDGE('',*,*,#3229,.F.);
#4320=ORIENTED_EDGE('',*,*,#3230,.F.);
#4321=ORIENTED_EDGE('',*,*,#3231,.T.);
#4322=ORIENTED_EDGE('',*,*,#3228,.T.);
#4323=ORIENTED_EDGE('',*,*,#3231,.F.);
#4324=ORIENTED_EDGE('',*,*,#3230,.T.);
#4325=ORIENTED_EDGE('',*,*,#3232,.F.);
#4326=ORIENTED_EDGE('',*,*,#3233,.F.);
#4327=ORIENTED_EDGE('',*,*,#3234,.T.);
#4328=ORIENTED_EDGE('',*,*,#3232,.T.);
#4329=ORIENTED_EDGE('',*,*,#3234,.F.);
#4330=ORIENTED_EDGE('',*,*,#3235,.F.);
#4331=ORIENTED_EDGE('',*,*,#3236,.T.);
#4332=ORIENTED_EDGE('',*,*,#3233,.T.);
#4333=ORIENTED_EDGE('',*,*,#3236,.F.);
#4334=ORIENTED_EDGE('',*,*,#3237,.F.);
#4335=ORIENTED_EDGE('',*,*,#3238,.T.);
#4336=ORIENTED_EDGE('',*,*,#3235,.T.);
#4337=ORIENTED_EDGE('',*,*,#3238,.F.);
#4338=ORIENTED_EDGE('',*,*,#3237,.T.);
#4339=ORIENTED_EDGE('',*,*,#3239,.T.);
#4340=ORIENTED_EDGE('',*,*,#3240,.T.);
#4341=ORIENTED_EDGE('',*,*,#3241,.T.);
#4342=ORIENTED_EDGE('',*,*,#3242,.F.);
#4343=ORIENTED_EDGE('',*,*,#3243,.T.);
#4344=ORIENTED_EDGE('',*,*,#3244,.T.);
#4345=ORIENTED_EDGE('',*,*,#3245,.T.);
#4346=ORIENTED_EDGE('',*,*,#3240,.F.);
#4347=ORIENTED_EDGE('',*,*,#3246,.T.);
#4348=ORIENTED_EDGE('',*,*,#3247,.T.);
#4349=ORIENTED_EDGE('',*,*,#3248,.T.);
#4350=ORIENTED_EDGE('',*,*,#3244,.F.);
#4351=ORIENTED_EDGE('',*,*,#3249,.T.);
#4352=ORIENTED_EDGE('',*,*,#3250,.T.);
#4353=ORIENTED_EDGE('',*,*,#3251,.T.);
#4354=ORIENTED_EDGE('',*,*,#3247,.F.);
#4355=ORIENTED_EDGE('',*,*,#3252,.T.);
#4356=ORIENTED_EDGE('',*,*,#3253,.T.);
#4357=ORIENTED_EDGE('',*,*,#3254,.T.);
#4358=ORIENTED_EDGE('',*,*,#3250,.F.);
#4359=ORIENTED_EDGE('',*,*,#3255,.T.);
#4360=ORIENTED_EDGE('',*,*,#3242,.T.);
#4361=ORIENTED_EDGE('',*,*,#3256,.T.);
#4362=ORIENTED_EDGE('',*,*,#3253,.F.);
#4363=ORIENTED_EDGE('',*,*,#3255,.F.);
#4364=ORIENTED_EDGE('',*,*,#3252,.F.);
#4365=ORIENTED_EDGE('',*,*,#3249,.F.);
#4366=ORIENTED_EDGE('',*,*,#3246,.F.);
#4367=ORIENTED_EDGE('',*,*,#3243,.F.);
#4368=ORIENTED_EDGE('',*,*,#3239,.F.);
#4369=ORIENTED_EDGE('',*,*,#3256,.F.);
#4370=ORIENTED_EDGE('',*,*,#3241,.F.);
#4371=ORIENTED_EDGE('',*,*,#3245,.F.);
#4372=ORIENTED_EDGE('',*,*,#3248,.F.);
#4373=ORIENTED_EDGE('',*,*,#3251,.F.);
#4374=ORIENTED_EDGE('',*,*,#3254,.F.);
#5218=CYLINDRICAL_SURFACE('',#6276,0.35);
#5219=CYLINDRICAL_SURFACE('',#6284,0.1954);
#5483=ADVANCED_FACE('',(#739),#519,.T.);
#5484=ADVANCED_FACE('',(#740),#231,.T.);
#5485=ADVANCED_FACE('',(#741),#5218,.T.);
#5486=ADVANCED_FACE('',(#742),#232,.T.);
#5487=ADVANCED_FACE('',(#743,#406),#520,.T.);
#5488=ADVANCED_FACE('',(#744),#233,.T.);
#5489=ADVANCED_FACE('',(#745),#5219,.T.);
#5490=ADVANCED_FACE('',(#746),#234,.T.);
#5491=ADVANCED_FACE('',(#747),#521,.T.);
#5492=ADVANCED_FACE('',(#748),#522,.F.);
#5493=ADVANCED_FACE('',(#749),#523,.F.);
#5494=ADVANCED_FACE('',(#750),#524,.F.);
#5495=ADVANCED_FACE('',(#751),#525,.F.);
#5496=ADVANCED_FACE('',(#752),#526,.F.);
#5497=ADVANCED_FACE('',(#753),#527,.F.);
#5498=ADVANCED_FACE('',(#754),#528,.F.);
#5499=ADVANCED_FACE('',(#755),#529,.F.);
#5673=CLOSED_SHELL('',(#5483,#5484,#5485,#5486,#5487,#5488,#5489,#5490,
#5491));
#5674=CLOSED_SHELL('',(#5492,#5493,#5494,#5495,#5496,#5497,#5498,#5499));
#6271=AXIS2_PLACEMENT_3D('',#9633,#7529,#7530);
#6272=AXIS2_PLACEMENT_3D('',#9634,#7531,#7532);
#6273=AXIS2_PLACEMENT_3D('',#9636,#7533,#7534);
#6274=AXIS2_PLACEMENT_3D('',#9637,#7535,#7536);
#6275=AXIS2_PLACEMENT_3D('',#9639,#7537,#7538);
#6276=AXIS2_PLACEMENT_3D('',#9641,#7540,#7541);
#6277=AXIS2_PLACEMENT_3D('',#9643,#7542,#7543);
#6278=AXIS2_PLACEMENT_3D('',#9645,#7545,#7546);
#6279=AXIS2_PLACEMENT_3D('',#9647,#7547,#7548);
#6280=AXIS2_PLACEMENT_3D('',#9649,#7550,#7551);
#6281=AXIS2_PLACEMENT_3D('',#9651,#7552,#7553);
#6282=AXIS2_PLACEMENT_3D('',#9652,#7554,#7555);
#6283=AXIS2_PLACEMENT_3D('',#9654,#7556,#7557);
#6284=AXIS2_PLACEMENT_3D('',#9656,#7559,#7560);
#6285=AXIS2_PLACEMENT_3D('',#9658,#7561,#7562);
#6286=AXIS2_PLACEMENT_3D('',#9660,#7564,#7565);
#6287=AXIS2_PLACEMENT_3D('',#9662,#7566,#7567);
#6288=AXIS2_PLACEMENT_3D('',#9664,#7569,#7570);
#6289=AXIS2_PLACEMENT_3D('',#9665,#7571,#7572);
#6290=AXIS2_PLACEMENT_3D('',#9674,#7577,#7578);
#6291=AXIS2_PLACEMENT_3D('',#9680,#7582,#7583);
#6292=AXIS2_PLACEMENT_3D('',#9686,#7587,#7588);
#6293=AXIS2_PLACEMENT_3D('',#9692,#7592,#7593);
#6294=AXIS2_PLACEMENT_3D('',#9698,#7597,#7598);
#6295=AXIS2_PLACEMENT_3D('',#9701,#7601,#7602);
#6296=AXIS2_PLACEMENT_3D('',#9702,#7603,#7604);
#7529=DIRECTION('axis',(0.,0.,1.));
#7530=DIRECTION('refdir',(1.,0.,0.));
#7531=DIRECTION('center_axis',(0.,1.,0.));
#7532=DIRECTION('ref_axis',(0.,0.,1.));
#7533=DIRECTION('center_axis',(0.,-1.,0.));
#7534=DIRECTION('ref_axis',(1.,0.,0.));
#7535=DIRECTION('center_axis',(0.,-1.,0.));
#7536=DIRECTION('ref_axis',(1.,0.,0.));
#7537=DIRECTION('center_axis',(0.,-1.,0.));
#7538=DIRECTION('ref_axis',(1.,0.,0.));
#7539=DIRECTION('',(0.707106781186547,0.707106781186548,8.65956056235493E-17));
#7540=DIRECTION('center_axis',(0.,-1.,0.));
#7541=DIRECTION('ref_axis',(1.,0.,0.));
#7542=DIRECTION('center_axis',(0.,-1.,0.));
#7543=DIRECTION('ref_axis',(1.,0.,0.));
#7544=DIRECTION('',(0.,1.,0.));
#7545=DIRECTION('center_axis',(0.,1.,0.));
#7546=DIRECTION('ref_axis',(1.,0.,0.));
#7547=DIRECTION('center_axis',(0.,-1.,0.));
#7548=DIRECTION('ref_axis',(1.,0.,0.));
#7549=DIRECTION('',(-0.707106781186547,0.707106781186548,-8.65956056235493E-17));
#7550=DIRECTION('center_axis',(0.,-1.,0.));
#7551=DIRECTION('ref_axis',(0.,0.,-1.));
#7552=DIRECTION('center_axis',(0.,-1.,0.));
#7553=DIRECTION('ref_axis',(1.,0.,0.));
#7554=DIRECTION('center_axis',(0.,1.,0.));
#7555=DIRECTION('ref_axis',(1.,0.,0.));
#7556=DIRECTION('center_axis',(0.,1.,0.));
#7557=DIRECTION('ref_axis',(1.,0.,0.));
#7558=DIRECTION('',(-0.447213595499958,0.894427190999916,-5.47678698264203E-17));
#7559=DIRECTION('center_axis',(0.,-1.,0.));
#7560=DIRECTION('ref_axis',(1.,0.,0.));
#7561=DIRECTION('center_axis',(0.,1.,0.));
#7562=DIRECTION('ref_axis',(1.,0.,0.));
#7563=DIRECTION('',(0.,1.,0.));
#7564=DIRECTION('center_axis',(0.,1.,0.));
#7565=DIRECTION('ref_axis',(1.,0.,0.));
#7566=DIRECTION('center_axis',(0.,-1.,0.));
#7567=DIRECTION('ref_axis',(1.,0.,0.));
#7568=DIRECTION('',(-0.707106781186547,0.707106781186548,-8.65956056235493E-17));
#7569=DIRECTION('center_axis',(0.,-1.,0.));
#7570=DIRECTION('ref_axis',(0.,0.,-1.));
#7571=DIRECTION('center_axis',(0.866025403784439,0.,-0.5));
#7572=DIRECTION('ref_axis',(0.5,0.,0.866025403784439));
#7573=DIRECTION('',(-0.5,0.,-0.866025403784439));
#7574=DIRECTION('',(0.,-1.,0.));
#7575=DIRECTION('',(0.5,0.,0.866025403784439));
#7576=DIRECTION('',(0.,-1.,0.));
#7577=DIRECTION('center_axis',(1.60246890531964E-16,0.,-1.));
#7578=DIRECTION('ref_axis',(1.,0.,1.60246890531964E-16));
#7579=DIRECTION('',(-1.,0.,-1.60246890531964E-16));
#7580=DIRECTION('',(0.,-1.,0.));
#7581=DIRECTION('',(1.,0.,1.60246890531964E-16));
#7582=DIRECTION('center_axis',(-0.866025403784439,0.,-0.5));
#7583=DIRECTION('ref_axis',(0.5,0.,-0.866025403784439));
#7584=DIRECTION('',(-0.5,0.,0.866025403784439));
#7585=DIRECTION('',(0.,-1.,0.));
#7586=DIRECTION('',(0.5,0.,-0.866025403784439));
#7587=DIRECTION('center_axis',(-0.866025403784439,0.,0.5));
#7588=DIRECTION('ref_axis',(-0.5,0.,-0.866025403784439));
#7589=DIRECTION('',(0.5,0.,0.866025403784439));
#7590=DIRECTION('',(0.,-1.,0.));
#7591=DIRECTION('',(-0.5,0.,-0.866025403784439));
#7592=DIRECTION('center_axis',(-1.60246890531964E-16,0.,1.));
#7593=DIRECTION('ref_axis',(-1.,0.,-1.60246890531964E-16));
#7594=DIRECTION('',(1.,0.,1.60246890531964E-16));
#7595=DIRECTION('',(0.,-1.,0.));
#7596=DIRECTION('',(-1.,0.,-1.60246890531964E-16));
#7597=DIRECTION('center_axis',(0.866025403784439,0.,0.5));
#7598=DIRECTION('ref_axis',(-0.5,0.,0.866025403784439));
#7599=DIRECTION('',(0.5,0.,-0.866025403784439));
#7600=DIRECTION('',(-0.5,0.,0.866025403784439));
#7601=DIRECTION('center_axis',(0.,1.,0.));
#7602=DIRECTION('ref_axis',(1.,0.,0.));
#7603=DIRECTION('center_axis',(0.,-1.,0.));
#7604=DIRECTION('ref_axis',(0.,0.,-1.));
#9633=CARTESIAN_POINT('',(0.,0.,0.));
#9634=CARTESIAN_POINT('Origin',(0.3,0.4,0.));
#9635=CARTESIAN_POINT('',(-0.3,0.4,-3.67394039744206E-17));
#9636=CARTESIAN_POINT('Origin',(0.,0.4,0.));
#9637=CARTESIAN_POINT('Origin',(0.,0.375,0.));
#9638=CARTESIAN_POINT('',(-0.35,0.35,-4.28626379701573E-17));
#9639=CARTESIAN_POINT('Origin',(0.,0.35,0.));
#9640=CARTESIAN_POINT('',(-0.325,0.375,-3.9801020972289E-17));
#9641=CARTESIAN_POINT('Origin',(0.,0.19,0.));
#9642=CARTESIAN_POINT('',(-0.35,0.03,-4.28626379701574E-17));
#9643=CARTESIAN_POINT('Origin',(0.,0.03,0.));
#9644=CARTESIAN_POINT('',(-0.35,0.19,-4.28626379701574E-17));
#9645=CARTESIAN_POINT('Origin',(0.,0.0149999999999999,0.));
#9646=CARTESIAN_POINT('',(-0.32,-3.29597460435593E-17,-3.91886975727153E-17));
#9647=CARTESIAN_POINT('Origin',(0.,0.,0.));
#9648=CARTESIAN_POINT('',(-0.335,0.0149999999999999,-4.10256677714363E-17));
#9649=CARTESIAN_POINT('Origin',(0.22,0.,0.));
#9650=CARTESIAN_POINT('',(-0.22,-6.93889390390723E-18,-2.69422295812418E-17));
#9651=CARTESIAN_POINT('Origin',(0.,0.,0.));
#9652=CARTESIAN_POINT('Origin',(0.,-0.02,0.));
#9653=CARTESIAN_POINT('',(-0.1954,-0.0492,2.39295984553393E-17));
#9654=CARTESIAN_POINT('Origin',(0.,-0.0492,0.));
#9655=CARTESIAN_POINT('',(-0.21,-0.02,-2.57175827820944E-17));
#9656=CARTESIAN_POINT('Origin',(0.,-0.8,0.));
#9657=CARTESIAN_POINT('',(-0.1954,-1.5646,2.39295984553393E-17));
#9658=CARTESIAN_POINT('Origin',(0.,-1.5646,0.));
#9659=CARTESIAN_POINT('',(-0.1954,-0.8,-2.39295984553393E-17));
#9660=CARTESIAN_POINT('Origin',(0.,-1.58,0.));
#9661=CARTESIAN_POINT('',(-0.16,-1.6,-1.95943487863577E-17));
#9662=CARTESIAN_POINT('Origin',(0.,-1.6,0.));
#9663=CARTESIAN_POINT('',(-0.18,-1.58,-2.20436423846524E-17));
#9664=CARTESIAN_POINT('Origin',(0.,-1.6,0.));
#9665=CARTESIAN_POINT('Origin',(0.0866025403784439,-0.4,-0.15));
#9666=CARTESIAN_POINT('',(0.173205080756888,-0.4,0.));
#9667=CARTESIAN_POINT('',(0.0866025403784439,-0.4,-0.15));
#9668=CARTESIAN_POINT('',(0.173205080756888,-0.4,0.));
#9669=CARTESIAN_POINT('',(0.0866025403784439,-0.64,-0.15));
#9670=CARTESIAN_POINT('',(0.0866025403784439,-0.4,-0.15));
#9671=CARTESIAN_POINT('',(0.173205080756888,-0.64,0.));
#9672=CARTESIAN_POINT('',(0.173205080756888,-0.64,0.));
#9673=CARTESIAN_POINT('',(0.173205080756888,-0.4,0.));
#9674=CARTESIAN_POINT('Origin',(-0.0866025403784438,-0.4,-0.15));
#9675=CARTESIAN_POINT('',(-0.0866025403784438,-0.4,-0.15));
#9676=CARTESIAN_POINT('',(0.0866025403784439,-0.4,-0.15));
#9677=CARTESIAN_POINT('',(-0.0866025403784438,-0.64,-0.15));
#9678=CARTESIAN_POINT('',(-0.0866025403784438,-0.4,-0.15));
#9679=CARTESIAN_POINT('',(0.0866025403784439,-0.64,-0.15));
#9680=CARTESIAN_POINT('Origin',(-0.173205080756888,-0.4,-2.77555756156289E-17));
#9681=CARTESIAN_POINT('',(-0.173205080756888,-0.4,-2.12115047744981E-17));
#9682=CARTESIAN_POINT('',(-0.0866025403784438,-0.4,-0.15));
#9683=CARTESIAN_POINT('',(-0.173205080756888,-0.64,-2.77555756156289E-17));
#9684=CARTESIAN_POINT('',(-0.173205080756888,-0.4,-2.12115047744981E-17));
#9685=CARTESIAN_POINT('',(-0.0866025403784438,-0.64,-0.15));
#9686=CARTESIAN_POINT('Origin',(-0.0866025403784439,-0.4,0.15));
#9687=CARTESIAN_POINT('',(-0.0866025403784439,-0.4,0.15));
#9688=CARTESIAN_POINT('',(-0.173205080756888,-0.4,-2.12115047744981E-17));
#9689=CARTESIAN_POINT('',(-0.0866025403784439,-0.64,0.15));
#9690=CARTESIAN_POINT('',(-0.0866025403784439,-0.4,0.15));
#9691=CARTESIAN_POINT('',(-0.173205080756888,-0.64,-2.12115047744981E-17));
#9692=CARTESIAN_POINT('Origin',(0.0866025403784439,-0.4,0.15));
#9693=CARTESIAN_POINT('',(0.0866025403784439,-0.4,0.15));
#9694=CARTESIAN_POINT('',(-0.0866025403784439,-0.4,0.15));
#9695=CARTESIAN_POINT('',(0.0866025403784439,-0.64,0.15));
#9696=CARTESIAN_POINT('',(0.0866025403784439,-0.4,0.15));
#9697=CARTESIAN_POINT('',(-0.0866025403784439,-0.64,0.15));
#9698=CARTESIAN_POINT('Origin',(0.173205080756888,-0.4,0.));
#9699=CARTESIAN_POINT('',(0.0866025403784439,-0.4,0.15));
#9700=CARTESIAN_POINT('',(0.0866025403784439,-0.64,0.15));
#9701=CARTESIAN_POINT('Origin',(0.,-0.4,-2.77555756156289E-17));
#9702=CARTESIAN_POINT('Origin',(0.,-0.64,-2.77555756156289E-17));
#10927=UNCERTAINTY_MEASURE_WITH_UNIT(LENGTH_MEASURE(0.001),#10964,
'DISTANCE_ACCURACY_VALUE',
'Maximum model space distance between geometric entities at asserted c
onnectivities');
#10936=UNCERTAINTY_MEASURE_WITH_UNIT(LENGTH_MEASURE(0.001),#10964,
'DISTANCE_ACCURACY_VALUE',
'Maximum model space distance between geometric entities at asserted c
onnectivities');
#10954=(
GEOMETRIC_REPRESENTATION_CONTEXT(3)
GLOBAL_UNCERTAINTY_ASSIGNED_CONTEXT((#10927))
GLOBAL_UNIT_ASSIGNED_CONTEXT((#10964,#10966,#10967))
REPRESENTATION_CONTEXT('','3D')
);
#10963=(
GEOMETRIC_REPRESENTATION_CONTEXT(3)
GLOBAL_UNCERTAINTY_ASSIGNED_CONTEXT((#10936))
GLOBAL_UNIT_ASSIGNED_CONTEXT((#10964,#10966,#10967))
REPRESENTATION_CONTEXT('','3D')
);
#10964=(
LENGTH_UNIT()
NAMED_UNIT(*)
SI_UNIT(.CENTI.,.METRE.)
);
#10966=(
NAMED_UNIT(*)
PLANE_ANGLE_UNIT()
SI_UNIT($,.RADIAN.)
);
#10967=(
NAMED_UNIT(*)
SI_UNIT($,.STERADIAN.)
SOLID_ANGLE_UNIT()
);
#10985=SHAPE_DEFINITION_REPRESENTATION(#11016,#11074);
#11016=PRODUCT_DEFINITION_SHAPE('',$,#11101);
#11074=SHAPE_REPRESENTATION('',(#6271),#10954);
#11083=PRODUCT_DEFINITION_CONTEXT('part definition',#11163,'design');
#11101=PRODUCT_DEFINITION('Cap Screw - M4x16','Cap Screw - M4x16',#11127,
#11083);
#11127=PRODUCT_DEFINITION_FORMATION('',$,#11182);
#11163=APPLICATION_CONTEXT(
'Core Data for Automotive Mechanical Design Process');
#11164=PRODUCT_CONTEXT('part definition',#11163,'mechanical');
#11182=PRODUCT('Cap Screw - M4x16','Cap Screw - M4x16',
'Cap Screw - M4x16',(#11164));
#11254=COLOUR_RGB('Black',0.12,0.14,0.17);
#11255=FILL_AREA_STYLE_COLOUR('',#11254);
#11256=FILL_AREA_STYLE('',(#11255));
#11257=SURFACE_STYLE_FILL_AREA(#11256);
#11258=SURFACE_SIDE_STYLE('',(#11257));
#11259=SURFACE_STYLE_USAGE(.BOTH.,#11258);
#11260=PRESENTATION_STYLE_ASSIGNMENT((#11259));
ENDSEC;
END-ISO-10303-21;
